ISO-10303-21;
HEADER;
FILE_DESCRIPTION (('STEP AP214'),
    '1' );
FILE_NAME ('12. Washer.step',
    '2026-10-09T08:13:37',
    ( '' ),
    ( '' ),
    'SwSTEP 2.0',
    'SolidWorks 2021',
    '' );
FILE_SCHEMA (( 'AUTOMOTIVE_DESIGN' ));
ENDSEC;

DATA;
#1190=PRODUCT_DEFINITION ( 'UNKNOWN', '', #57360, #55755 ) ;
#1220=ORIENTED_EDGE ( 'NONE', *, *, #65094, .T. ) ;
#1962=CARTESIAN_POINT ( 'NONE',  ( 6.123233995736766282E-16, 0.000000000000000000, 5.000000000000000000 ) ) ;
#2253=LINE ( 'NONE', #23780, #38963 ) ;
#2438=CIRCLE ( 'NONE', #59790, 10.00000000000000000 ) ;
#2490=ORIENTED_EDGE ( 'NONE', *, *, #24499, .F. ) ;
#2591=CIRCLE ( 'NONE', #12727, 10.00000000000000000 ) ;
#2629=DIRECTION ( 'NONE',  ( -0.000000000000000000, -1.000000000000000000, -0.000000000000000000 ) ) ;
#2797=PRESENTATION_STYLE_ASSIGNMENT (( #55255 ) ) ;
#3231=DIRECTION ( 'NONE',  ( 0.000000000000000000, 1.000000000000000000, 0.000000000000000000 ) ) ;
#3256=VERTEX_POINT ( 'NONE', #15747 ) ;
#3549=ORIENTED_EDGE ( 'NONE', *, *, #57663, .T. ) ;
#3585=ORIENTED_EDGE ( 'NONE', *, *, #28305, .T. ) ;
#3655=CLOSED_SHELL ( 'NONE', ( #48585, #66169, #58525, #44594, #38181, #11191 ) ) ;
#4568=EDGE_CURVE ( 'NONE', #49089, #40754, #35853, .T. ) ;
#4719=FACE_OUTER_BOUND ( 'NONE', #65087, .T. ) ;
#4759=DIRECTION ( 'NONE',  ( 0.000000000000000000, 0.000000000000000000, -1.000000000000000000 ) ) ;
#5297=CYLINDRICAL_SURFACE ( 'NONE', #57738, 10.00000000000000000 ) ;
#5481=AXIS2_PLACEMENT_3D ( 'NONE', #38191, #37518, #43139 ) ;
#5931=CIRCLE ( 'NONE', #50893, 10.00000000000000000 ) ;
#6289=EDGE_LOOP ( 'NONE', ( #33546, #3585 ) ) ;
#7217=DIRECTION ( 'NONE',  ( 0.000000000000000000, 0.000000000000000000, 1.000000000000000000 ) ) ;
#7506=DIRECTION ( 'NONE',  ( -0.000000000000000000, -1.000000000000000000, -0.000000000000000000 ) ) ;
#7887=CARTESIAN_POINT ( 'NONE',  ( 0.000000000000000000, 2.299999999999999822, -10.00000000000000000 ) ) ;
#8126=FILL_AREA_STYLE_COLOUR ( '', #33310 ) ;
#8220=DIRECTION ( 'NONE',  ( -0.000000000000000000, -1.000000000000000000, -0.000000000000000000 ) ) ;
#8438=VECTOR ( 'NONE', #7506, 1000.000000000000000 ) ;
#8953=ORIENTED_EDGE ( 'NONE', *, *, #22185, .F. ) ;
#9256=ORIENTED_EDGE ( 'NONE', *, *, #57663, .F. ) ;
#9725=PRODUCT_DEFINITION_SHAPE ( 'NONE', 'NONE',  #1190 ) ;
#9846=ORIENTED_EDGE ( 'NONE', *, *, #24499, .T. ) ;
#10061=CYLINDRICAL_SURFACE ( 'NONE', #45875, 10.00000000000000000 ) ;
#10226=ORIENTED_EDGE ( 'NONE', *, *, #41727, .F. ) ;
#10258=SURFACE_STYLE_USAGE ( .BOTH. , #20084 ) ;
#11191=ADVANCED_FACE ( 'NONE', ( #53487 ), #68628, .F. ) ;
#11620=CARTESIAN_POINT ( 'NONE',  ( 0.000000000000000000, 0.000000000000000000, 0.000000000000000000 ) ) ;
#12132=PRODUCT_CONTEXT ( 'NONE', #14129, 'mechanical' ) ;
#12727=AXIS2_PLACEMENT_3D ( 'NONE', #28908, #27527, #28563 ) ;
#12785=DIRECTION ( 'NONE',  ( 0.000000000000000000, 0.000000000000000000, 1.000000000000000000 ) ) ;
#12927=CARTESIAN_POINT ( 'NONE',  ( 0.000000000000000000, 2.299999999999999822, 0.000000000000000000 ) ) ;
#13774=EDGE_LOOP ( 'NONE', ( #28052, #41845 ) ) ;
#13978=DIRECTION ( 'NONE',  ( 0.000000000000000000, 1.000000000000000000, 0.000000000000000000 ) ) ;
#14083=ORIENTED_EDGE ( 'NONE', *, *, #67914, .F. ) ;
#14129=APPLICATION_CONTEXT ( 'automotive_design' ) ;
#14283=CARTESIAN_POINT ( 'NONE',  ( 1.224646799147353256E-15, 0.000000000000000000, 10.00000000000000000 ) ) ;
#14304=UNCERTAINTY_MEASURE_WITH_UNIT (LENGTH_MEASURE( 1.000000000000000082E-05 ), #23991, 'distance_accuracy_value', 'NONE');
#14756=VERTEX_POINT ( 'NONE', #14283 ) ;
#15007=DIRECTION ( 'NONE',  ( -0.000000000000000000, -1.000000000000000000, -0.000000000000000000 ) ) ;
#15196=DIRECTION ( 'NONE',  ( 0.000000000000000000, 0.000000000000000000, -1.000000000000000000 ) ) ;
#15228=DIRECTION ( 'NONE',  ( 0.000000000000000000, 0.000000000000000000, -1.000000000000000000 ) ) ;
#15455=AXIS2_PLACEMENT_3D ( 'NONE', #46043, #41117, #68175 ) ;
#15689=CARTESIAN_POINT ( 'NONE',  ( 0.000000000000000000, 2.299999999999999822, 0.000000000000000000 ) ) ;
#15727=AXIS2_PLACEMENT_3D ( 'NONE', #51474, #3231, #31050 ) ;
#15746=STYLED_ITEM ( 'NONE', ( #47231 ), #47271 ) ;
#15747=CARTESIAN_POINT ( 'NONE',  ( 0.000000000000000000, 0.000000000000000000, -10.00000000000000000 ) ) ;
#15893=( NAMED_UNIT ( * ) SI_UNIT ( $, .STERADIAN. ) SOLID_ANGLE_UNIT ( ) );
#16253=( NAMED_UNIT ( * ) PLANE_ANGLE_UNIT ( ) SI_UNIT ( $, .RADIAN. ) );
#16465=DIRECTION ( 'NONE',  ( 0.000000000000000000, 1.000000000000000000, 0.000000000000000000 ) ) ;
#16563=EDGE_LOOP ( 'NONE', ( #24680, #29601, #3549, #33129 ) ) ;
#18382=CARTESIAN_POINT ( 'NONE',  ( 0.000000000000000000, 0.000000000000000000, 0.000000000000000000 ) ) ;
#19214=UNCERTAINTY_MEASURE_WITH_UNIT (LENGTH_MEASURE( 1.000000000000000082E-05 ), #26735, 'distance_accuracy_value', 'NONE');
#19513=EDGE_LOOP ( 'NONE', ( #35461, #1220, #34036, #2490 ) ) ;
#20084=SURFACE_SIDE_STYLE ('',( #53834 ) ) ;
#20430=CARTESIAN_POINT ( 'NONE',  ( 0.000000000000000000, 2.299999999999999822, 0.000000000000000000 ) ) ;
#21747=SHAPE_REPRESENTATION ( '12. Washer', ( #42840 ), #24690 ) ;
#22059=( GEOMETRIC_REPRESENTATION_CONTEXT ( 3 ) GLOBAL_UNCERTAINTY_ASSIGNED_CONTEXT ( ( #25703 ) ) GLOBAL_UNIT_ASSIGNED_CONTEXT ( ( #23943, #56293, #56658 ) ) REPRESENTATION_CONTEXT ( 'NONE', 'WORKASPACE' ) );
#22185=EDGE_CURVE ( 'NONE', #43827, #28053, #2438, .T. ) ;
#23780=CARTESIAN_POINT ( 'NONE',  ( 1.224646799147353256E-15, 2.299999999999999822, 10.00000000000000000 ) ) ;
#23943=( LENGTH_UNIT ( ) NAMED_UNIT ( * ) SI_UNIT ( .MILLI., .METRE. ) );
#23991=( LENGTH_UNIT ( ) NAMED_UNIT ( * ) SI_UNIT ( .MILLI., .METRE. ) );
#24499=EDGE_CURVE ( 'NONE', #43827, #3256, #40237, .T. ) ;
#24670=EDGE_LOOP ( 'NONE', ( #42175, #30258 ) ) ;
#24680=ORIENTED_EDGE ( 'NONE', *, *, #43201, .F. ) ;
#24690=( GEOMETRIC_REPRESENTATION_CONTEXT ( 3 ) GLOBAL_UNCERTAINTY_ASSIGNED_CONTEXT ( ( #14304 ) ) GLOBAL_UNIT_ASSIGNED_CONTEXT ( ( #23991, #16253, #63006 ) ) REPRESENTATION_CONTEXT ( 'NONE', 'WORKASPACE' ) );
#25703=UNCERTAINTY_MEASURE_WITH_UNIT (LENGTH_MEASURE( 1.000000000000000082E-05 ), #23943, 'distance_accuracy_value', 'NONE');
#25708=FILL_AREA_STYLE ('',( #27083 ) ) ;
#25827=AXIS2_PLACEMENT_3D ( 'NONE', #11620, #65067, #33086 ) ;
#26155=CARTESIAN_POINT ( 'NONE',  ( 0.000000000000000000, 2.299999999999999822, 0.000000000000000000 ) ) ;
#26552=PRODUCT ( '12. Washer', '12. Washer', '', ( #12132 ) ) ;
#26561=MECHANICAL_DESIGN_GEOMETRIC_PRESENTATION_REPRESENTATION('',(#56902),#22059);
#26735=( LENGTH_UNIT ( ) NAMED_UNIT ( * ) SI_UNIT ( .MILLI., .METRE. ) );
#27083=FILL_AREA_STYLE_COLOUR ( '', #40516 ) ;
#27527=DIRECTION ( 'NONE',  ( 0.000000000000000000, 1.000000000000000000, 0.000000000000000000 ) ) ;
#28052=ORIENTED_EDGE ( 'NONE', *, *, #37863, .F. ) ;
#28053=VERTEX_POINT ( 'NONE', #30964 ) ;
#28305=EDGE_CURVE ( 'NONE', #28053, #43827, #42933, .T. ) ;
#28563=DIRECTION ( 'NONE',  ( 0.000000000000000000, 0.000000000000000000, 1.000000000000000000 ) ) ;
#28908=CARTESIAN_POINT ( 'NONE',  ( 0.000000000000000000, 0.000000000000000000, 0.000000000000000000 ) ) ;
#28932=CARTESIAN_POINT ( 'NONE',  ( 0.000000000000000000, 2.299999999999999822, -5.000000000000000000 ) ) ;
#29478=FACE_BOUND ( 'NONE', #33701, .T. ) ;
#29601=ORIENTED_EDGE ( 'NONE', *, *, #37804, .T. ) ;
#30251=CIRCLE ( 'NONE', #15727, 5.000000000000000000 ) ;
#30258=ORIENTED_EDGE ( 'NONE', *, *, #4568, .T. ) ;
#30386=DIRECTION ( 'NONE',  ( -0.000000000000000000, -1.000000000000000000, -0.000000000000000000 ) ) ;
#30513=DIRECTION ( 'NONE',  ( 0.000000000000000000, 0.000000000000000000, 1.000000000000000000 ) ) ;
#30964=CARTESIAN_POINT ( 'NONE',  ( 1.224646799147353256E-15, 2.299999999999999822, 10.00000000000000000 ) ) ;
#31050=DIRECTION ( 'NONE',  ( 0.000000000000000000, 0.000000000000000000, 1.000000000000000000 ) ) ;
#31481=( GEOMETRIC_REPRESENTATION_CONTEXT ( 3 ) GLOBAL_UNCERTAINTY_ASSIGNED_CONTEXT ( ( #19214 ) ) GLOBAL_UNIT_ASSIGNED_CONTEXT ( ( #26735, #37374, #15893 ) ) REPRESENTATION_CONTEXT ( 'NONE', 'WORKASPACE' ) );
#32046=SHAPE_REPRESENTATION_RELATIONSHIP ( 'NONE' , 'NONE' ,  #21747, #47271 ) ;
#33086=DIRECTION ( 'NONE',  ( 0.000000000000000000, -0.000000000000000000, 1.000000000000000000 ) ) ;
#33129=ORIENTED_EDGE ( 'NONE', *, *, #4568, .F. ) ;
#33310=COLOUR_RGB ( '', 0.09019608, 0.27058824, 0.51372549) ;
#33546=ORIENTED_EDGE ( 'NONE', *, *, #22185, .T. ) ;
#33701=EDGE_LOOP ( 'NONE', ( #10226, #59543 ) ) ;
#34036=ORIENTED_EDGE ( 'NONE', *, *, #46834, .T. ) ;
#34392=DIRECTION ( 'NONE',  ( 0.000000000000000000, 0.000000000000000000, 1.000000000000000000 ) ) ;
#34534=DIRECTION ( 'NONE',  ( 0.000000000000000000, 1.000000000000000000, 0.000000000000000000 ) ) ;
#34940=CARTESIAN_POINT ( 'NONE',  ( 0.000000000000000000, 2.299999999999999822, -10.00000000000000000 ) ) ;
#35198=SURFACE_STYLE_FILL_AREA ( #40503 ) ;
#35230=LINE ( 'NONE', #40888, #48178 ) ;
#35461=ORIENTED_EDGE ( 'NONE', *, *, #28305, .F. ) ;
#35853=CIRCLE ( 'NONE', #5481, 5.000000000000000000 ) ;
#37374=( NAMED_UNIT ( * ) PLANE_ANGLE_UNIT ( ) SI_UNIT ( $, .RADIAN. ) );
#37518=DIRECTION ( 'NONE',  ( 0.000000000000000000, 1.000000000000000000, 0.000000000000000000 ) ) ;
#37804=EDGE_CURVE ( 'NONE', #66680, #52777, #62176, .T. ) ;
#37819=DIRECTION ( 'NONE',  ( 0.000000000000000000, 1.000000000000000000, 0.000000000000000000 ) ) ;
#37863=EDGE_CURVE ( 'NONE', #3256, #14756, #2591, .T. ) ;
#38023=CIRCLE ( 'NONE', #47016, 5.000000000000000000 ) ;
#38181=ADVANCED_FACE ( 'NONE', ( #69351 ), #5297, .T. ) ;
#38191=CARTESIAN_POINT ( 'NONE',  ( 0.000000000000000000, 0.000000000000000000, 0.000000000000000000 ) ) ;
#38483=ORIENTED_EDGE ( 'NONE', *, *, #41727, .T. ) ;
#38963=VECTOR ( 'NONE', #2629, 1000.000000000000000 ) ;
#39867=DIRECTION ( 'NONE',  ( 0.000000000000000000, 0.000000000000000000, 1.000000000000000000 ) ) ;
#40237=LINE ( 'NONE', #34940, #60907 ) ;
#40503=FILL_AREA_STYLE ('',( #8126 ) ) ;
#40516=COLOUR_RGB ( '', 0.09019608, 0.27058824, 0.51372549) ;
#40642=APPLICATION_CONTEXT ( 'automotive_design' ) ;
#40754=VERTEX_POINT ( 'NONE', #54568 ) ;
#40888=CARTESIAN_POINT ( 'NONE',  ( 6.123233995736766282E-16, 2.299999999999999822, 5.000000000000000000 ) ) ;
#41117=DIRECTION ( 'NONE',  ( 0.000000000000000000, 1.000000000000000000, 0.000000000000000000 ) ) ;
#41617=MECHANICAL_DESIGN_GEOMETRIC_PRESENTATION_REPRESENTATION('',(#15746),#31481);
#41727=EDGE_CURVE ( 'NONE', #52777, #66680, #30251, .T. ) ;
#41845=ORIENTED_EDGE ( 'NONE', *, *, #46834, .F. ) ;
#42175=ORIENTED_EDGE ( 'NONE', *, *, #67914, .T. ) ;
#42327=DIRECTION ( 'NONE',  ( -0.000000000000000000, -1.000000000000000000, -0.000000000000000000 ) ) ;
#42840=AXIS2_PLACEMENT_3D ( 'NONE', #59977, #7217, #49786 ) ;
#42933=CIRCLE ( 'NONE', #66482, 10.00000000000000000 ) ;
#43139=DIRECTION ( 'NONE',  ( 0.000000000000000000, 0.000000000000000000, 1.000000000000000000 ) ) ;
#43201=EDGE_CURVE ( 'NONE', #66680, #49089, #35230, .T. ) ;
#43676=PLANE ( 'NONE',  #25827 ) ;
#43827=VERTEX_POINT ( 'NONE', #7887 ) ;
#44594=ADVANCED_FACE ( 'NONE', ( #54177, #59808 ), #43676, .F. ) ;
#44890=SHAPE_DEFINITION_REPRESENTATION ( #9725, #21747 ) ;
#45106=SURFACE_SIDE_STYLE ('',( #35198 ) ) ;
#45875=AXIS2_PLACEMENT_3D ( 'NONE', #15689, #15007, #4759 ) ;
#46043=CARTESIAN_POINT ( 'NONE',  ( 0.000000000000000000, 2.299999999999999822, 0.000000000000000000 ) ) ;
#46654=DIRECTION ( 'NONE',  ( 0.000000000000000000, 0.000000000000000000, -1.000000000000000000 ) ) ;
#46834=EDGE_CURVE ( 'NONE', #14756, #3256, #5931, .T. ) ;
#47016=AXIS2_PLACEMENT_3D ( 'NONE', #18382, #34534, #39867 ) ;
#47231=PRESENTATION_STYLE_ASSIGNMENT (( #10258 ) ) ;
#47271=ADVANCED_BREP_SHAPE_REPRESENTATION ( '', ( #50161, #42840 ), #24690 ) ;
#48178=VECTOR ( 'NONE', #52478, 1000.000000000000000 ) ;
#48585=ADVANCED_FACE ( 'NONE', ( #4719 ), #68402, .F. ) ;
#49089=VERTEX_POINT ( 'NONE', #1962 ) ;
#49786=DIRECTION ( 'NONE',  ( 1.000000000000000000, 0.000000000000000000, 0.000000000000000000 ) ) ;
#50161=MANIFOLD_SOLID_BREP ( 'Boss-Extrude1', #3655 ) ;
#50751=ORIENTED_EDGE ( 'NONE', *, *, #37863, .T. ) ;
#50893=AXIS2_PLACEMENT_3D ( 'NONE', #69538, #16465, #12785 ) ;
#51474=CARTESIAN_POINT ( 'NONE',  ( 0.000000000000000000, 2.299999999999999822, 0.000000000000000000 ) ) ;
#51652=DIRECTION ( 'NONE',  ( 0.000000000000000000, 1.000000000000000000, 0.000000000000000000 ) ) ;
#52355=PLANE ( 'NONE',  #15455 ) ;
#52478=DIRECTION ( 'NONE',  ( -0.000000000000000000, -1.000000000000000000, -0.000000000000000000 ) ) ;
#52777=VERTEX_POINT ( 'NONE', #61442 ) ;
#53487=FACE_OUTER_BOUND ( 'NONE', #16563, .T. ) ;
#53834=SURFACE_STYLE_FILL_AREA ( #25708 ) ;
#54177=FACE_OUTER_BOUND ( 'NONE', #13774, .T. ) ;
#54568=CARTESIAN_POINT ( 'NONE',  ( 0.000000000000000000, 0.000000000000000000, -5.000000000000000000 ) ) ;
#55255=SURFACE_STYLE_USAGE ( .BOTH. , #45106 ) ;
#55363=ORIENTED_EDGE ( 'NONE', *, *, #43201, .T. ) ;
#55755=PRODUCT_DEFINITION_CONTEXT ( 'detailed design', #40642, 'design' ) ;
#56293=( NAMED_UNIT ( * ) PLANE_ANGLE_UNIT ( ) SI_UNIT ( $, .RADIAN. ) );
#56658=( NAMED_UNIT ( * ) SI_UNIT ( $, .STERADIAN. ) SOLID_ANGLE_UNIT ( ) );
#56902=STYLED_ITEM ( 'NONE', ( #2797 ), #50161 ) ;
#57360=PRODUCT_DEFINITION_FORMATION_WITH_SPECIFIED_SOURCE ( 'ANY', '', #26552, .NOT_KNOWN. ) ;
#57663=EDGE_CURVE ( 'NONE', #52777, #40754, #66599, .T. ) ;
#57738=AXIS2_PLACEMENT_3D ( 'NONE', #69685, #42327, #15228 ) ;
#58525=ADVANCED_FACE ( 'NONE', ( #67822, #29478 ), #52355, .T. ) ;
#59543=ORIENTED_EDGE ( 'NONE', *, *, #37804, .F. ) ;
#59790=AXIS2_PLACEMENT_3D ( 'NONE', #12927, #13978, #34392 ) ;
#59808=FACE_BOUND ( 'NONE', #24670, .T. ) ;
#59977=CARTESIAN_POINT ( 'NONE',  ( 0.000000000000000000, 0.000000000000000000, 0.000000000000000000 ) ) ;
#60907=VECTOR ( 'NONE', #8220, 1000.000000000000000 ) ;
#61442=CARTESIAN_POINT ( 'NONE',  ( 0.000000000000000000, 2.299999999999999822, -5.000000000000000000 ) ) ;
#61770=AXIS2_PLACEMENT_3D ( 'NONE', #20430, #63341, #15196 ) ;
#62176=CIRCLE ( 'NONE', #66667, 5.000000000000000000 ) ;
#62282=AXIS2_PLACEMENT_3D ( 'NONE', #68072, #30386, #46654 ) ;
#62342=EDGE_LOOP ( 'NONE', ( #63675, #8953, #9846, #50751 ) ) ;
#62537=CARTESIAN_POINT ( 'NONE',  ( 0.000000000000000000, 2.299999999999999822, 0.000000000000000000 ) ) ;
#63006=( NAMED_UNIT ( * ) SI_UNIT ( $, .STERADIAN. ) SOLID_ANGLE_UNIT ( ) );
#63341=DIRECTION ( 'NONE',  ( -0.000000000000000000, -1.000000000000000000, -0.000000000000000000 ) ) ;
#63675=ORIENTED_EDGE ( 'NONE', *, *, #65094, .F. ) ;
#63844=FACE_OUTER_BOUND ( 'NONE', #19513, .T. ) ;
#64835=DIRECTION ( 'NONE',  ( 0.000000000000000000, 0.000000000000000000, 1.000000000000000000 ) ) ;
#65067=DIRECTION ( 'NONE',  ( 0.000000000000000000, 1.000000000000000000, 0.000000000000000000 ) ) ;
#65087=EDGE_LOOP ( 'NONE', ( #38483, #55363, #14083, #9256 ) ) ;
#65094=EDGE_CURVE ( 'NONE', #28053, #14756, #2253, .T. ) ;
#66169=ADVANCED_FACE ( 'NONE', ( #63844 ), #10061, .T. ) ;
#66482=AXIS2_PLACEMENT_3D ( 'NONE', #62537, #51652, #30513 ) ;
#66599=LINE ( 'NONE', #28932, #8438 ) ;
#66667=AXIS2_PLACEMENT_3D ( 'NONE', #26155, #37819, #64835 ) ;
#66680=VERTEX_POINT ( 'NONE', #69408 ) ;
#67822=FACE_OUTER_BOUND ( 'NONE', #6289, .T. ) ;
#67914=EDGE_CURVE ( 'NONE', #40754, #49089, #38023, .T. ) ;
#68072=CARTESIAN_POINT ( 'NONE',  ( 0.000000000000000000, 2.299999999999999822, 0.000000000000000000 ) ) ;
#68175=DIRECTION ( 'NONE',  ( 0.000000000000000000, -0.000000000000000000, 1.000000000000000000 ) ) ;
#68402=CYLINDRICAL_SURFACE ( 'NONE', #62282, 5.000000000000000000 ) ;
#68628=CYLINDRICAL_SURFACE ( 'NONE', #61770, 5.000000000000000000 ) ;
#69351=FACE_OUTER_BOUND ( 'NONE', #62342, .T. ) ;
#69408=CARTESIAN_POINT ( 'NONE',  ( 6.123233995736766282E-16, 2.299999999999999822, 5.000000000000000000 ) ) ;
#69538=CARTESIAN_POINT ( 'NONE',  ( 0.000000000000000000, 0.000000000000000000, 0.000000000000000000 ) ) ;
#69685=CARTESIAN_POINT ( 'NONE',  ( 0.000000000000000000, 2.299999999999999822, 0.000000000000000000 ) ) ;
ENDSEC;
END-ISO-10303-21;
